ISO-10303-21;
HEADER;
/* Generated by software containing ST-Developer
 * from STEP Tools, Inc. (www.steptools.com) 
 */

FILE_DESCRIPTION(
/* description */ ('Belt tensioner idler arm'),
/* implementation_level */ '2;1');

FILE_NAME(
/* name */ 'Stop screw bracket.step',
/* time_stamp */ '2026-10-28T03:22:15-07:00',
/* author */ (''),
/* organization */ (''),
/* preprocessor_version */ 'ST-DEVELOPER v20.2',
/* originating_system */ 'Autodesk Translation Framework v15.17.0.0',
/* authorisation */ '');

FILE_SCHEMA (('AUTOMOTIVE_DESIGN { 1 0 10303 214 3 1 1 }'));
ENDSEC;

DATA;
#10=MECHANICAL_DESIGN_GEOMETRIC_PRESENTATION_REPRESENTATION('',(#454),#12779);
#386=SHAPE_REPRESENTATION_RELATIONSHIP('SRR','None',#12932,#420);
#420=ADVANCED_BREP_SHAPE_REPRESENTATION('',(#496),#12749);
#454=STYLED_ITEM('',(#13191),#496);
#496=MANIFOLD_SOLID_BREP('Body1',#6188);
#553=FACE_BOUND('',#1294,.T.);
#554=FACE_BOUND('',#1297,.T.);
#555=FACE_BOUND('',#1301,.T.);
#701=PLANE('',#6719);
#702=PLANE('',#6723);
#703=PLANE('',#6724);
#704=PLANE('',#6725);
#705=PLANE('',#6726);
#706=PLANE('',#6727);
#707=PLANE('',#6728);
#897=FACE_OUTER_BOUND('',#1290,.T.);
#898=FACE_OUTER_BOUND('',#1291,.T.);
#899=FACE_OUTER_BOUND('',#1292,.T.);
#900=FACE_OUTER_BOUND('',#1293,.T.);
#901=FACE_OUTER_BOUND('',#1295,.T.);
#902=FACE_OUTER_BOUND('',#1296,.T.);
#903=FACE_OUTER_BOUND('',#1298,.T.);
#904=FACE_OUTER_BOUND('',#1299,.T.);
#905=FACE_OUTER_BOUND('',#1300,.T.);
#1290=EDGE_LOOP('',(#4324,#4325,#4326,#4327));
#1291=EDGE_LOOP('',(#4328));
#1292=EDGE_LOOP('',(#4329,#4330,#4331,#4332));
#1293=EDGE_LOOP('',(#4333,#4334,#4335,#4336));
#1294=EDGE_LOOP('',(#4337));
#1295=EDGE_LOOP('',(#4338,#4339,#4340,#4341));
#1296=EDGE_LOOP('',(#4342,#4343,#4344,#4345));
#1297=EDGE_LOOP('',(#4346));
#1298=EDGE_LOOP('',(#4347,#4348,#4349,#4350));
#1299=EDGE_LOOP('',(#4351,#4352,#4353,#4354));
#1300=EDGE_LOOP('',(#4355,#4356,#4357,#4358));
#1301=EDGE_LOOP('',(#4359));
#1769=LINE('',#10416,#2118);
#1770=LINE('',#10423,#2119);
#1771=LINE('',#10428,#2120);
#1772=LINE('',#10430,#2121);
#1773=LINE('',#10432,#2122);
#1774=LINE('',#10433,#2123);
#1775=LINE('',#10436,#2124);
#1776=LINE('',#10438,#2125);
#1777=LINE('',#10439,#2126);
#1778=LINE('',#10442,#2127);
#1779=LINE('',#10444,#2128);
#1780=LINE('',#10445,#2129);
#1781=LINE('',#10447,#2130);
#1782=LINE('',#10448,#2131);
#2118=VECTOR('',#7727,0.165);
#2119=VECTOR('',#7736,0.21);
#2120=VECTOR('',#7741,1.);
#2121=VECTOR('',#7742,1.);
#2122=VECTOR('',#7743,1.);
#2123=VECTOR('',#7744,1.);
#2124=VECTOR('',#7747,1.);
#2125=VECTOR('',#7748,1.);
#2126=VECTOR('',#7749,1.);
#2127=VECTOR('',#7752,1.);
#2128=VECTOR('',#7753,1.);
#2129=VECTOR('',#7754,1.);
#2130=VECTOR('',#7757,1.);
#2131=VECTOR('',#7758,1.);
#2449=CIRCLE('',#6717,0.165);
#2450=CIRCLE('',#6718,0.165);
#2451=CIRCLE('',#6721,0.21);
#2452=CIRCLE('',#6722,0.21);
#2846=VERTEX_POINT('',#10413);
#2847=VERTEX_POINT('',#10415);
#2848=VERTEX_POINT('',#10420);
#2849=VERTEX_POINT('',#10422);
#2850=VERTEX_POINT('',#10426);
#2851=VERTEX_POINT('',#10427);
#2852=VERTEX_POINT('',#10429);
#2853=VERTEX_POINT('',#10431);
#2854=VERTEX_POINT('',#10435);
#2855=VERTEX_POINT('',#10437);
#2856=VERTEX_POINT('',#10441);
#2857=VERTEX_POINT('',#10443);
#3417=EDGE_CURVE('',#2846,#2846,#2449,.T.);
#3418=EDGE_CURVE('',#2846,#2847,#1769,.T.);
#3419=EDGE_CURVE('',#2847,#2847,#2450,.T.);
#3420=EDGE_CURVE('',#2848,#2848,#2451,.T.);
#3421=EDGE_CURVE('',#2848,#2849,#1770,.T.);
#3422=EDGE_CURVE('',#2849,#2849,#2452,.T.);
#3423=EDGE_CURVE('',#2850,#2851,#1771,.T.);
#3424=EDGE_CURVE('',#2851,#2852,#1772,.T.);
#3425=EDGE_CURVE('',#2853,#2852,#1773,.T.);
#3426=EDGE_CURVE('',#2850,#2853,#1774,.T.);
#3427=EDGE_CURVE('',#2854,#2850,#1775,.T.);
#3428=EDGE_CURVE('',#2855,#2853,#1776,.T.);
#3429=EDGE_CURVE('',#2854,#2855,#1777,.T.);
#3430=EDGE_CURVE('',#2856,#2854,#1778,.T.);
#3431=EDGE_CURVE('',#2857,#2855,#1779,.T.);
#3432=EDGE_CURVE('',#2856,#2857,#1780,.T.);
#3433=EDGE_CURVE('',#2851,#2856,#1781,.T.);
#3434=EDGE_CURVE('',#2852,#2857,#1782,.T.);
#4324=ORIENTED_EDGE('',*,*,#3417,.F.);
#4325=ORIENTED_EDGE('',*,*,#3418,.T.);
#4326=ORIENTED_EDGE('',*,*,#3419,.T.);
#4327=ORIENTED_EDGE('',*,*,#3418,.F.);
#4328=ORIENTED_EDGE('',*,*,#3419,.F.);
#4329=ORIENTED_EDGE('',*,*,#3420,.F.);
#4330=ORIENTED_EDGE('',*,*,#3421,.T.);
#4331=ORIENTED_EDGE('',*,*,#3422,.F.);
#4332=ORIENTED_EDGE('',*,*,#3421,.F.);
#4333=ORIENTED_EDGE('',*,*,#3423,.T.);
#4334=ORIENTED_EDGE('',*,*,#3424,.T.);
#4335=ORIENTED_EDGE('',*,*,#3425,.F.);
#4336=ORIENTED_EDGE('',*,*,#3426,.F.);
#4337=ORIENTED_EDGE('',*,*,#3422,.T.);
#4338=ORIENTED_EDGE('',*,*,#3427,.T.);
#4339=ORIENTED_EDGE('',*,*,#3426,.T.);
#4340=ORIENTED_EDGE('',*,*,#3428,.F.);
#4341=ORIENTED_EDGE('',*,*,#3429,.F.);
#4342=ORIENTED_EDGE('',*,*,#3430,.T.);
#4343=ORIENTED_EDGE('',*,*,#3429,.T.);
#4344=ORIENTED_EDGE('',*,*,#3431,.F.);
#4345=ORIENTED_EDGE('',*,*,#3432,.F.);
#4346=ORIENTED_EDGE('',*,*,#3420,.T.);
#4347=ORIENTED_EDGE('',*,*,#3433,.T.);
#4348=ORIENTED_EDGE('',*,*,#3432,.T.);
#4349=ORIENTED_EDGE('',*,*,#3434,.F.);
#4350=ORIENTED_EDGE('',*,*,#3424,.F.);
#4351=ORIENTED_EDGE('',*,*,#3434,.T.);
#4352=ORIENTED_EDGE('',*,*,#3431,.T.);
#4353=ORIENTED_EDGE('',*,*,#3428,.T.);
#4354=ORIENTED_EDGE('',*,*,#3425,.T.);
#4355=ORIENTED_EDGE('',*,*,#3433,.F.);
#4356=ORIENTED_EDGE('',*,*,#3423,.F.);
#4357=ORIENTED_EDGE('',*,*,#3427,.F.);
#4358=ORIENTED_EDGE('',*,*,#3430,.F.);
#4359=ORIENTED_EDGE('',*,*,#3417,.T.);
#5683=CYLINDRICAL_SURFACE('',#6716,0.165);
#5684=CYLINDRICAL_SURFACE('',#6720,0.21);
#5874=ADVANCED_FACE('',(#897),#5683,.F.);
#5875=ADVANCED_FACE('',(#898),#701,.F.);
#5876=ADVANCED_FACE('',(#899),#5684,.F.);
#5877=ADVANCED_FACE('',(#900,#553),#702,.T.);
#5878=ADVANCED_FACE('',(#901),#703,.T.);
#5879=ADVANCED_FACE('',(#902,#554),#704,.T.);
#5880=ADVANCED_FACE('',(#903),#705,.T.);
#5881=ADVANCED_FACE('',(#904),#706,.T.);
#5882=ADVANCED_FACE('',(#905,#555),#707,.F.);
#6188=CLOSED_SHELL('',(#5874,#5875,#5876,#5877,#5878,#5879,#5880,#5881,
#5882));
#6715=AXIS2_PLACEMENT_3D('',#10411,#7721,#7722);
#6716=AXIS2_PLACEMENT_3D('',#10412,#7723,#7724);
#6717=AXIS2_PLACEMENT_3D('',#10414,#7725,#7726);
#6718=AXIS2_PLACEMENT_3D('',#10417,#7728,#7729);
#6719=AXIS2_PLACEMENT_3D('',#10418,#7730,#7731);
#6720=AXIS2_PLACEMENT_3D('',#10419,#7732,#7733);
#6721=AXIS2_PLACEMENT_3D('',#10421,#7734,#7735);
#6722=AXIS2_PLACEMENT_3D('',#10424,#7737,#7738);
#6723=AXIS2_PLACEMENT_3D('',#10425,#7739,#7740);
#6724=AXIS2_PLACEMENT_3D('',#10434,#7745,#7746);
#6725=AXIS2_PLACEMENT_3D('',#10440,#7750,#7751);
#6726=AXIS2_PLACEMENT_3D('',#10446,#7755,#7756);
#6727=AXIS2_PLACEMENT_3D('',#10449,#7759,#7760);
#6728=AXIS2_PLACEMENT_3D('',#10450,#7761,#7762);
#7721=DIRECTION('axis',(0.,0.,1.));
#7722=DIRECTION('refdir',(1.,0.,0.));
#7723=DIRECTION('center_axis',(0.,0.,1.));
#7724=DIRECTION('ref_axis',(1.,0.,0.));
#7725=DIRECTION('center_axis',(0.,0.,1.));
#7726=DIRECTION('ref_axis',(1.,0.,0.));
#7727=DIRECTION('',(0.,0.,1.));
#7728=DIRECTION('center_axis',(0.,0.,1.));
#7729=DIRECTION('ref_axis',(1.,0.,0.));
#7730=DIRECTION('center_axis',(0.,0.,1.));
#7731=DIRECTION('ref_axis',(1.,0.,0.));
#7732=DIRECTION('center_axis',(0.,1.,0.));
#7733=DIRECTION('ref_axis',(1.,0.,0.));
#7734=DIRECTION('center_axis',(0.,1.,0.));
#7735=DIRECTION('ref_axis',(1.,0.,0.));
#7736=DIRECTION('',(0.,1.,0.));
#7737=DIRECTION('center_axis',(0.,-1.,0.));
#7738=DIRECTION('ref_axis',(1.,0.,0.));
#7739=DIRECTION('center_axis',(0.,1.,0.));
#7740=DIRECTION('ref_axis',(-1.,0.,0.));
#7741=DIRECTION('',(-1.,0.,0.));
#7742=DIRECTION('',(0.,0.,1.));
#7743=DIRECTION('',(-1.,0.,0.));
#7744=DIRECTION('',(0.,0.,1.));
#7745=DIRECTION('center_axis',(1.,0.,0.));
#7746=DIRECTION('ref_axis',(0.,1.,0.));
#7747=DIRECTION('',(0.,1.,0.));
#7748=DIRECTION('',(0.,1.,0.));
#7749=DIRECTION('',(0.,0.,1.));
#7750=DIRECTION('center_axis',(0.,-1.,0.));
#7751=DIRECTION('ref_axis',(1.,0.,0.));
#7752=DIRECTION('',(1.,0.,0.));
#7753=DIRECTION('',(1.,0.,0.));
#7754=DIRECTION('',(0.,0.,1.));
#7755=DIRECTION('center_axis',(-1.,0.,0.));
#7756=DIRECTION('ref_axis',(0.,-1.,0.));
#7757=DIRECTION('',(0.,-1.,0.));
#7758=DIRECTION('',(0.,-1.,0.));
#7759=DIRECTION('center_axis',(0.,0.,1.));
#7760=DIRECTION('ref_axis',(1.,0.,0.));
#7761=DIRECTION('center_axis',(0.,0.,1.));
#7762=DIRECTION('ref_axis',(1.,0.,0.));
#10411=CARTESIAN_POINT('',(0.,0.,0.));
#10412=CARTESIAN_POINT('Origin',(6.,1.9,-0.1));
#10413=CARTESIAN_POINT('',(5.835,1.9,0.));
#10414=CARTESIAN_POINT('Origin',(6.,1.9,0.));
#10415=CARTESIAN_POINT('',(5.835,1.9,1.1));
#10416=CARTESIAN_POINT('',(5.835,1.9,-0.1));
#10417=CARTESIAN_POINT('Origin',(6.,1.9,1.1));
#10418=CARTESIAN_POINT('Origin',(6.,1.9,1.1));
#10419=CARTESIAN_POINT('Origin',(6.,1.4,5.5));
#10420=CARTESIAN_POINT('',(5.79,1.5,5.5));
#10421=CARTESIAN_POINT('Origin',(6.,1.5,5.5));
#10422=CARTESIAN_POINT('',(5.79,2.3,5.5));
#10423=CARTESIAN_POINT('',(5.79,1.4,5.5));
#10424=CARTESIAN_POINT('Origin',(6.,2.3,5.5));
#10425=CARTESIAN_POINT('Origin',(7.,2.3,0.));
#10426=CARTESIAN_POINT('',(7.,2.3,0.));
#10427=CARTESIAN_POINT('',(5.,2.3,0.));
#10428=CARTESIAN_POINT('',(7.,2.3,0.));
#10429=CARTESIAN_POINT('',(5.,2.3,6.5));
#10430=CARTESIAN_POINT('',(5.,2.3,0.));
#10431=CARTESIAN_POINT('',(7.,2.3,6.5));
#10432=CARTESIAN_POINT('',(7.,2.3,6.5));
#10433=CARTESIAN_POINT('',(7.,2.3,0.));
#10434=CARTESIAN_POINT('Origin',(7.,1.5,0.));
#10435=CARTESIAN_POINT('',(7.,1.5,0.));
#10436=CARTESIAN_POINT('',(7.,1.5,0.));
#10437=CARTESIAN_POINT('',(7.,1.5,6.5));
#10438=CARTESIAN_POINT('',(7.,1.5,6.5));
#10439=CARTESIAN_POINT('',(7.,1.5,0.));
#10440=CARTESIAN_POINT('Origin',(5.,1.5,0.));
#10441=CARTESIAN_POINT('',(5.,1.5,0.));
#10442=CARTESIAN_POINT('',(5.,1.5,0.));
#10443=CARTESIAN_POINT('',(5.,1.5,6.5));
#10444=CARTESIAN_POINT('',(5.,1.5,6.5));
#10445=CARTESIAN_POINT('',(5.,1.5,0.));
#10446=CARTESIAN_POINT('Origin',(5.,2.3,0.));
#10447=CARTESIAN_POINT('',(5.,2.3,0.));
#10448=CARTESIAN_POINT('',(5.,2.3,6.5));
#10449=CARTESIAN_POINT('Origin',(6.,1.9,6.5));
#10450=CARTESIAN_POINT('Origin',(6.,1.9,0.));
#12709=UNCERTAINTY_MEASURE_WITH_UNIT(LENGTH_MEASURE(0.001),#12780,
'DISTANCE_ACCURACY_VALUE',
'Maximum model space distance between geometric entities at asserted c
onnectivities');
#12739=UNCERTAINTY_MEASURE_WITH_UNIT(LENGTH_MEASURE(0.001),#12780,
'DISTANCE_ACCURACY_VALUE',
'Maximum model space distance between geometric entities at asserted c
onnectivities');
#12749=(
GEOMETRIC_REPRESENTATION_CONTEXT(3)
GLOBAL_UNCERTAINTY_ASSIGNED_CONTEXT((#12709))
GLOBAL_UNIT_ASSIGNED_CONTEXT((#12780,#12782,#12783))
REPRESENTATION_CONTEXT('','3D')
);
#12779=(
GEOMETRIC_REPRESENTATION_CONTEXT(3)
GLOBAL_UNCERTAINTY_ASSIGNED_CONTEXT((#12739))
GLOBAL_UNIT_ASSIGNED_CONTEXT((#12780,#12782,#12783))
REPRESENTATION_CONTEXT('','3D')
);
#12780=(
LENGTH_UNIT()
NAMED_UNIT(*)
SI_UNIT(.CENTI.,.METRE.)
);
#12782=(
NAMED_UNIT(*)
PLANE_ANGLE_UNIT()
SI_UNIT($,.RADIAN.)
);
#12783=(
NAMED_UNIT(*)
SI_UNIT($,.STERADIAN.)
SOLID_ANGLE_UNIT()
);
#12793=SHAPE_DEFINITION_REPRESENTATION(#12832,#12932);
#12832=PRODUCT_DEFINITION_SHAPE('',$,#12972);
#12932=SHAPE_REPRESENTATION('',(#6715),#12749);
#12962=PRODUCT_DEFINITION_CONTEXT('part definition',#13081,'design');
#12972=PRODUCT_DEFINITION('Stop screw bracket','Stop screw bracket',#13011,
#12962);
#13011=PRODUCT_DEFINITION_FORMATION('',$,#13092);
#13081=APPLICATION_CONTEXT(
'Core Data for Automotive Mechanical Design Process');
#13082=PRODUCT_CONTEXT('part definition',#13081,'mechanical');
#13092=PRODUCT('Stop screw bracket','Stop screw bracket',
'Stop screw bracket',(#13082));
#13185=COLOUR_RGB('Black',0.12,0.14,0.17);
#13186=FILL_AREA_STYLE_COLOUR('',#13185);
#13187=FILL_AREA_STYLE('',(#13186));
#13188=SURFACE_STYLE_FILL_AREA(#13187);
#13189=SURFACE_SIDE_STYLE('',(#13188));
#13190=SURFACE_STYLE_USAGE(.BOTH.,#13189);
#13191=PRESENTATION_STYLE_ASSIGNMENT((#13190));
ENDSEC;
END-ISO-10303-21;
